ISO-10303-21;
HEADER;
/* Generated by software containing ST-Developer
 * from STEP Tools, Inc. (www.steptools.com) 
 */

FILE_DESCRIPTION(
/* description */ (''),
/* implementation_level */ '2;1');

FILE_NAME(
/* name */ 'Pivot thrust washer.step',
/* time_stamp */ '2026-11-10T05:40:20-08:00',
/* author */ (''),
/* organization */ (''),
/* preprocessor_version */ 'ST-DEVELOPER v20.2',
/* originating_system */ 'Autodesk Translation Framework v15.17.0.0',
/* authorisation */ '');

FILE_SCHEMA (('AUTOMOTIVE_DESIGN { 1 0 10303 214 3 1 1 }'));
ENDSEC;

DATA;
#10=MECHANICAL_DESIGN_GEOMETRIC_PRESENTATION_REPRESENTATION('',(#580),#18580);
#562=SHAPE_REPRESENTATION_RELATIONSHIP('SRR','None',#18633,#571);
#571=ADVANCED_BREP_SHAPE_REPRESENTATION('',(#589),#18579);
#580=STYLED_ITEM('',(#18689),#589);
#589=MANIFOLD_SOLID_BREP('Body1',#6552);
#649=FACE_BOUND('',#1606,.T.);
#650=FACE_BOUND('',#1608,.T.);
#794=PLANE('',#7124);
#795=PLANE('',#7125);
#1168=FACE_OUTER_BOUND('',#1603,.T.);
#1169=FACE_OUTER_BOUND('',#1604,.T.);
#1170=FACE_OUTER_BOUND('',#1605,.T.);
#1171=FACE_OUTER_BOUND('',#1607,.T.);
#1603=EDGE_LOOP('',(#6022,#6023,#6024,#6025));
#1604=EDGE_LOOP('',(#6026,#6027,#6028,#6029));
#1605=EDGE_LOOP('',(#6030));
#1606=EDGE_LOOP('',(#6031));
#1607=EDGE_LOOP('',(#6032));
#1608=EDGE_LOOP('',(#6033));
#2014=LINE('',#18539,#2421);
#2015=LINE('',#18545,#2422);
#2421=VECTOR('',#8473,0.41);
#2422=VECTOR('',#8480,0.6);
#2577=CIRCLE('',#7119,0.41);
#2578=CIRCLE('',#7120,0.41);
#2579=CIRCLE('',#7122,0.6);
#2580=CIRCLE('',#7123,0.6);
#3189=VERTEX_POINT('',#18536);
#3190=VERTEX_POINT('',#18538);
#3191=VERTEX_POINT('',#18542);
#3192=VERTEX_POINT('',#18544);
#4134=EDGE_CURVE('',#3189,#3189,#2577,.T.);
#4135=EDGE_CURVE('',#3189,#3190,#2014,.T.);
#4136=EDGE_CURVE('',#3190,#3190,#2578,.T.);
#4137=EDGE_CURVE('',#3191,#3191,#2579,.T.);
#4138=EDGE_CURVE('',#3191,#3192,#2015,.T.);
#4139=EDGE_CURVE('',#3192,#3192,#2580,.T.);
#6022=ORIENTED_EDGE('',*,*,#4134,.F.);
#6023=ORIENTED_EDGE('',*,*,#4135,.T.);
#6024=ORIENTED_EDGE('',*,*,#4136,.T.);
#6025=ORIENTED_EDGE('',*,*,#4135,.F.);
#6026=ORIENTED_EDGE('',*,*,#4137,.F.);
#6027=ORIENTED_EDGE('',*,*,#4138,.T.);
#6028=ORIENTED_EDGE('',*,*,#4139,.T.);
#6029=ORIENTED_EDGE('',*,*,#4138,.F.);
#6030=ORIENTED_EDGE('',*,*,#4137,.T.);
#6031=ORIENTED_EDGE('',*,*,#4134,.T.);
#6032=ORIENTED_EDGE('',*,*,#4139,.F.);
#6033=ORIENTED_EDGE('',*,*,#4136,.F.);
#6166=CYLINDRICAL_SURFACE('',#7118,0.41);
#6167=CYLINDRICAL_SURFACE('',#7121,0.6);
#6540=ADVANCED_FACE('',(#1168),#6166,.F.);
#6541=ADVANCED_FACE('',(#1169),#6167,.T.);
#6542=ADVANCED_FACE('',(#1170,#649),#794,.T.);
#6543=ADVANCED_FACE('',(#1171,#650),#795,.F.);
#6552=CLOSED_SHELL('',(#6540,#6541,#6542,#6543));
#7117=AXIS2_PLACEMENT_3D('',#18534,#8467,#8468);
#7118=AXIS2_PLACEMENT_3D('',#18535,#8469,#8470);
#7119=AXIS2_PLACEMENT_3D('',#18537,#8471,#8472);
#7120=AXIS2_PLACEMENT_3D('',#18540,#8474,#8475);
#7121=AXIS2_PLACEMENT_3D('',#18541,#8476,#8477);
#7122=AXIS2_PLACEMENT_3D('',#18543,#8478,#8479);
#7123=AXIS2_PLACEMENT_3D('',#18546,#8481,#8482);
#7124=AXIS2_PLACEMENT_3D('',#18547,#8483,#8484);
#7125=AXIS2_PLACEMENT_3D('',#18548,#8485,#8486);
#8467=DIRECTION('axis',(0.,0.,1.));
#8468=DIRECTION('refdir',(1.,0.,0.));
#8469=DIRECTION('center_axis',(0.,0.,1.));
#8470=DIRECTION('ref_axis',(1.,0.,0.));
#8471=DIRECTION('center_axis',(0.,0.,-1.));
#8472=DIRECTION('ref_axis',(1.,0.,0.));
#8473=DIRECTION('',(0.,0.,-1.));
#8474=DIRECTION('center_axis',(0.,0.,-1.));
#8475=DIRECTION('ref_axis',(1.,0.,0.));
#8476=DIRECTION('center_axis',(0.,0.,1.));
#8477=DIRECTION('ref_axis',(1.,0.,0.));
#8478=DIRECTION('center_axis',(0.,0.,1.));
#8479=DIRECTION('ref_axis',(1.,0.,0.));
#8480=DIRECTION('',(0.,0.,-1.));
#8481=DIRECTION('center_axis',(0.,0.,1.));
#8482=DIRECTION('ref_axis',(1.,0.,0.));
#8483=DIRECTION('center_axis',(0.,0.,1.));
#8484=DIRECTION('ref_axis',(1.,0.,0.));
#8485=DIRECTION('center_axis',(0.,0.,1.));
#8486=DIRECTION('ref_axis',(1.,0.,0.));
#18534=CARTESIAN_POINT('',(0.,0.,0.));
#18535=CARTESIAN_POINT('Origin',(0.,0.,0.));
#18536=CARTESIAN_POINT('',(-0.41,-5.02105187650415E-17,0.1));
#18537=CARTESIAN_POINT('Origin',(0.,0.,0.1));
#18538=CARTESIAN_POINT('',(-0.41,-5.02105187650415E-17,0.));
#18539=CARTESIAN_POINT('',(-0.41,-5.02105187650415E-17,0.));
#18540=CARTESIAN_POINT('Origin',(0.,0.,0.));
#18541=CARTESIAN_POINT('Origin',(0.,0.,0.));
#18542=CARTESIAN_POINT('',(-0.6,-7.34788079488412E-17,0.1));
#18543=CARTESIAN_POINT('Origin',(0.,0.,0.1));
#18544=CARTESIAN_POINT('',(-0.6,-7.34788079488412E-17,0.));
#18545=CARTESIAN_POINT('',(-0.6,-7.34788079488412E-17,0.));
#18546=CARTESIAN_POINT('Origin',(0.,0.,0.));
#18547=CARTESIAN_POINT('Origin',(0.,0.,0.1));
#18548=CARTESIAN_POINT('Origin',(0.,0.,0.));
#18567=UNCERTAINTY_MEASURE_WITH_UNIT(LENGTH_MEASURE(0.001),#18581,
'DISTANCE_ACCURACY_VALUE',
'Maximum model space distance between geometric entities at asserted c
onnectivities');
#18568=UNCERTAINTY_MEASURE_WITH_UNIT(LENGTH_MEASURE(0.001),#18581,
'DISTANCE_ACCURACY_VALUE',
'Maximum model space distance between geometric entities at asserted c
onnectivities');
#18579=(
GEOMETRIC_REPRESENTATION_CONTEXT(3)
GLOBAL_UNCERTAINTY_ASSIGNED_CONTEXT((#18567))
GLOBAL_UNIT_ASSIGNED_CONTEXT((#18581,#18583,#18584))
REPRESENTATION_CONTEXT('','3D')
);
#18580=(
GEOMETRIC_REPRESENTATION_CONTEXT(3)
GLOBAL_UNCERTAINTY_ASSIGNED_CONTEXT((#18568))
GLOBAL_UNIT_ASSIGNED_CONTEXT((#18581,#18583,#18584))
REPRESENTATION_CONTEXT('','3D')
);
#18581=(
LENGTH_UNIT()
NAMED_UNIT(*)
SI_UNIT(.CENTI.,.METRE.)
);
#18583=(
NAMED_UNIT(*)
PLANE_ANGLE_UNIT()
SI_UNIT($,.RADIAN.)
);
#18584=(
NAMED_UNIT(*)
SI_UNIT($,.STERADIAN.)
SOLID_ANGLE_UNIT()
);
#18595=SHAPE_DEFINITION_REPRESENTATION(#18614,#18633);
#18614=PRODUCT_DEFINITION_SHAPE('',$,#18645);
#18633=SHAPE_REPRESENTATION('',(#7117),#18579);
#18634=PRODUCT_DEFINITION_CONTEXT('part definition',#18669,'design');
#18645=PRODUCT_DEFINITION('Pivot thrust washer','Pivot thrust washer',#18656,
#18634);
#18656=PRODUCT_DEFINITION_FORMATION('',$,#18681);
#18669=APPLICATION_CONTEXT(
'Core Data for Automotive Mechanical Design Process');
#18670=PRODUCT_CONTEXT('part definition',#18669,'mechanical');
#18681=PRODUCT('Pivot thrust washer','Pivot thrust washer',$,(#18670));
#18689=PRESENTATION_STYLE_ASSIGNMENT((#18697));
#18697=SURFACE_STYLE_USAGE(.BOTH.,#18705);
#18705=SURFACE_SIDE_STYLE('',(#18713));
#18713=SURFACE_STYLE_FILL_AREA(#18721);
#18721=FILL_AREA_STYLE('Washer gray',(#18729));
#18729=FILL_AREA_STYLE_COLOUR('Washer gray',#18737);
#18737=COLOUR_RGB('Washer gray',0.725490196078431,0.752941176470588,0.792156862745098);
ENDSEC;
END-ISO-10303-21;
